ISO-10303-21;
HEADER;
/* Generated by software containing ST-Developer
 * from STEP Tools, Inc. (www.steptools.com) 
 */

FILE_DESCRIPTION(
/* description */ ('PAT-083'),
/* implementation_level */ '2;1');

FILE_NAME(
/* name */ 'Foot pad (1).step',
/* time_stamp */ '2026-10-29T20:18:00-07:00',
/* author */ (''),
/* organization */ (''),
/* preprocessor_version */ 'ST-DEVELOPER v20.2',
/* originating_system */ 'Autodesk Translation Framework v15.17.0.0',
/* authorisation */ '');

FILE_SCHEMA (('AUTOMOTIVE_DESIGN { 1 0 10303 214 3 1 1 }'));
ENDSEC;

DATA;
#10=MECHANICAL_DESIGN_GEOMETRIC_PRESENTATION_REPRESENTATION('',(#246),#8428);
#198=SHAPE_REPRESENTATION_RELATIONSHIP('SRR','None',#8532,#222);
#222=ADVANCED_BREP_SHAPE_REPRESENTATION('',(#270),#8421);
#246=STYLED_ITEM('',(#8698),#270);
#270=MANIFOLD_SOLID_BREP('Body1',#3692);
#438=PLANE('',#4281);
#439=PLANE('',#4282);
#440=PLANE('',#4283);
#441=PLANE('',#4284);
#442=PLANE('',#4285);
#443=PLANE('',#4286);
#646=FACE_OUTER_BOUND('',#949,.T.);
#647=FACE_OUTER_BOUND('',#950,.T.);
#648=FACE_OUTER_BOUND('',#951,.T.);
#649=FACE_OUTER_BOUND('',#952,.T.);
#650=FACE_OUTER_BOUND('',#953,.T.);
#651=FACE_OUTER_BOUND('',#954,.T.);
#949=EDGE_LOOP('',(#3038,#3039,#3040,#3041));
#950=EDGE_LOOP('',(#3042,#3043,#3044,#3045));
#951=EDGE_LOOP('',(#3046,#3047,#3048,#3049));
#952=EDGE_LOOP('',(#3050,#3051,#3052,#3053));
#953=EDGE_LOOP('',(#3054,#3055,#3056,#3057));
#954=EDGE_LOOP('',(#3058,#3059,#3060,#3061));
#1171=LINE('',#7970,#1415);
#1172=LINE('',#7972,#1416);
#1173=LINE('',#7974,#1417);
#1174=LINE('',#7975,#1418);
#1175=LINE('',#7978,#1419);
#1176=LINE('',#7980,#1420);
#1177=LINE('',#7981,#1421);
#1178=LINE('',#7984,#1422);
#1179=LINE('',#7986,#1423);
#1180=LINE('',#7987,#1424);
#1181=LINE('',#7989,#1425);
#1182=LINE('',#7990,#1426);
#1415=VECTOR('',#5197,1.);
#1416=VECTOR('',#5198,1.);
#1417=VECTOR('',#5199,1.);
#1418=VECTOR('',#5200,1.);
#1419=VECTOR('',#5203,1.);
#1420=VECTOR('',#5204,1.);
#1421=VECTOR('',#5205,1.);
#1422=VECTOR('',#5208,1.);
#1423=VECTOR('',#5209,1.);
#1424=VECTOR('',#5210,1.);
#1425=VECTOR('',#5213,1.);
#1426=VECTOR('',#5214,1.);
#1901=VERTEX_POINT('',#7968);
#1902=VERTEX_POINT('',#7969);
#1903=VERTEX_POINT('',#7971);
#1904=VERTEX_POINT('',#7973);
#1905=VERTEX_POINT('',#7977);
#1906=VERTEX_POINT('',#7979);
#1907=VERTEX_POINT('',#7983);
#1908=VERTEX_POINT('',#7985);
#2295=EDGE_CURVE('',#1901,#1902,#1171,.T.);
#2296=EDGE_CURVE('',#1902,#1903,#1172,.T.);
#2297=EDGE_CURVE('',#1904,#1903,#1173,.T.);
#2298=EDGE_CURVE('',#1901,#1904,#1174,.T.);
#2299=EDGE_CURVE('',#1905,#1901,#1175,.T.);
#2300=EDGE_CURVE('',#1906,#1904,#1176,.T.);
#2301=EDGE_CURVE('',#1905,#1906,#1177,.T.);
#2302=EDGE_CURVE('',#1907,#1905,#1178,.T.);
#2303=EDGE_CURVE('',#1908,#1906,#1179,.T.);
#2304=EDGE_CURVE('',#1907,#1908,#1180,.T.);
#2305=EDGE_CURVE('',#1902,#1907,#1181,.T.);
#2306=EDGE_CURVE('',#1903,#1908,#1182,.T.);
#3038=ORIENTED_EDGE('',*,*,#2295,.T.);
#3039=ORIENTED_EDGE('',*,*,#2296,.T.);
#3040=ORIENTED_EDGE('',*,*,#2297,.F.);
#3041=ORIENTED_EDGE('',*,*,#2298,.F.);
#3042=ORIENTED_EDGE('',*,*,#2299,.T.);
#3043=ORIENTED_EDGE('',*,*,#2298,.T.);
#3044=ORIENTED_EDGE('',*,*,#2300,.F.);
#3045=ORIENTED_EDGE('',*,*,#2301,.F.);
#3046=ORIENTED_EDGE('',*,*,#2302,.T.);
#3047=ORIENTED_EDGE('',*,*,#2301,.T.);
#3048=ORIENTED_EDGE('',*,*,#2303,.F.);
#3049=ORIENTED_EDGE('',*,*,#2304,.F.);
#3050=ORIENTED_EDGE('',*,*,#2305,.T.);
#3051=ORIENTED_EDGE('',*,*,#2304,.T.);
#3052=ORIENTED_EDGE('',*,*,#2306,.F.);
#3053=ORIENTED_EDGE('',*,*,#2296,.F.);
#3054=ORIENTED_EDGE('',*,*,#2306,.T.);
#3055=ORIENTED_EDGE('',*,*,#2303,.T.);
#3056=ORIENTED_EDGE('',*,*,#2300,.T.);
#3057=ORIENTED_EDGE('',*,*,#2297,.T.);
#3058=ORIENTED_EDGE('',*,*,#2305,.F.);
#3059=ORIENTED_EDGE('',*,*,#2295,.F.);
#3060=ORIENTED_EDGE('',*,*,#2299,.F.);
#3061=ORIENTED_EDGE('',*,*,#2302,.F.);
#3593=ADVANCED_FACE('',(#646),#438,.T.);
#3594=ADVANCED_FACE('',(#647),#439,.T.);
#3595=ADVANCED_FACE('',(#648),#440,.T.);
#3596=ADVANCED_FACE('',(#649),#441,.T.);
#3597=ADVANCED_FACE('',(#650),#442,.T.);
#3598=ADVANCED_FACE('',(#651),#443,.F.);
#3692=CLOSED_SHELL('',(#3593,#3594,#3595,#3596,#3597,#3598));
#4280=AXIS2_PLACEMENT_3D('',#7966,#5193,#5194);
#4281=AXIS2_PLACEMENT_3D('',#7967,#5195,#5196);
#4282=AXIS2_PLACEMENT_3D('',#7976,#5201,#5202);
#4283=AXIS2_PLACEMENT_3D('',#7982,#5206,#5207);
#4284=AXIS2_PLACEMENT_3D('',#7988,#5211,#5212);
#4285=AXIS2_PLACEMENT_3D('',#7991,#5215,#5216);
#4286=AXIS2_PLACEMENT_3D('',#7992,#5217,#5218);
#5193=DIRECTION('axis',(0.,0.,1.));
#5194=DIRECTION('refdir',(1.,0.,0.));
#5195=DIRECTION('center_axis',(0.,1.,0.));
#5196=DIRECTION('ref_axis',(-1.,0.,0.));
#5197=DIRECTION('',(-1.,0.,0.));
#5198=DIRECTION('',(0.,0.,1.));
#5199=DIRECTION('',(-1.,0.,0.));
#5200=DIRECTION('',(0.,0.,1.));
#5201=DIRECTION('center_axis',(1.,0.,0.));
#5202=DIRECTION('ref_axis',(0.,1.,0.));
#5203=DIRECTION('',(0.,1.,0.));
#5204=DIRECTION('',(0.,1.,0.));
#5205=DIRECTION('',(0.,0.,1.));
#5206=DIRECTION('center_axis',(0.,-1.,0.));
#5207=DIRECTION('ref_axis',(1.,0.,0.));
#5208=DIRECTION('',(1.,0.,0.));
#5209=DIRECTION('',(1.,0.,0.));
#5210=DIRECTION('',(0.,0.,1.));
#5211=DIRECTION('center_axis',(-1.,0.,0.));
#5212=DIRECTION('ref_axis',(0.,-1.,0.));
#5213=DIRECTION('',(0.,-1.,0.));
#5214=DIRECTION('',(0.,-1.,0.));
#5215=DIRECTION('center_axis',(0.,0.,1.));
#5216=DIRECTION('ref_axis',(1.,0.,0.));
#5217=DIRECTION('center_axis',(0.,0.,1.));
#5218=DIRECTION('ref_axis',(1.,0.,0.));
#7966=CARTESIAN_POINT('',(0.,0.,0.));
#7967=CARTESIAN_POINT('Origin',(6.,4.5,-0.6));
#7968=CARTESIAN_POINT('',(6.,4.5,-0.6));
#7969=CARTESIAN_POINT('',(4.,4.5,-0.6));
#7970=CARTESIAN_POINT('',(6.,4.5,-0.6));
#7971=CARTESIAN_POINT('',(4.,4.5,0.));
#7972=CARTESIAN_POINT('',(4.,4.5,-0.6));
#7973=CARTESIAN_POINT('',(6.,4.5,0.));
#7974=CARTESIAN_POINT('',(6.,4.5,0.));
#7975=CARTESIAN_POINT('',(6.,4.5,-0.6));
#7976=CARTESIAN_POINT('Origin',(6.,-4.5,-0.6));
#7977=CARTESIAN_POINT('',(6.,-4.5,-0.6));
#7978=CARTESIAN_POINT('',(6.,-4.5,-0.6));
#7979=CARTESIAN_POINT('',(6.,-4.5,0.));
#7980=CARTESIAN_POINT('',(6.,-4.5,0.));
#7981=CARTESIAN_POINT('',(6.,-4.5,-0.6));
#7982=CARTESIAN_POINT('Origin',(4.,-4.5,-0.6));
#7983=CARTESIAN_POINT('',(4.,-4.5,-0.6));
#7984=CARTESIAN_POINT('',(4.,-4.5,-0.6));
#7985=CARTESIAN_POINT('',(4.,-4.5,0.));
#7986=CARTESIAN_POINT('',(4.,-4.5,0.));
#7987=CARTESIAN_POINT('',(4.,-4.5,-0.6));
#7988=CARTESIAN_POINT('Origin',(4.,4.5,-0.6));
#7989=CARTESIAN_POINT('',(4.,4.5,-0.6));
#7990=CARTESIAN_POINT('',(4.,4.5,0.));
#7991=CARTESIAN_POINT('Origin',(5.,0.,0.));
#7992=CARTESIAN_POINT('Origin',(5.,0.,-0.6));
#8395=UNCERTAINTY_MEASURE_WITH_UNIT(LENGTH_MEASURE(0.001),#8429,
'DISTANCE_ACCURACY_VALUE',
'Maximum model space distance between geometric entities at asserted c
onnectivities');
#8402=UNCERTAINTY_MEASURE_WITH_UNIT(LENGTH_MEASURE(0.001),#8429,
'DISTANCE_ACCURACY_VALUE',
'Maximum model space distance between geometric entities at asserted c
onnectivities');
#8421=(
GEOMETRIC_REPRESENTATION_CONTEXT(3)
GLOBAL_UNCERTAINTY_ASSIGNED_CONTEXT((#8395))
GLOBAL_UNIT_ASSIGNED_CONTEXT((#8429,#8431,#8432))
REPRESENTATION_CONTEXT('','3D')
);
#8428=(
GEOMETRIC_REPRESENTATION_CONTEXT(3)
GLOBAL_UNCERTAINTY_ASSIGNED_CONTEXT((#8402))
GLOBAL_UNIT_ASSIGNED_CONTEXT((#8429,#8431,#8432))
REPRESENTATION_CONTEXT('','3D')
);
#8429=(
LENGTH_UNIT()
NAMED_UNIT(*)
SI_UNIT(.CENTI.,.METRE.)
);
#8431=(
NAMED_UNIT(*)
PLANE_ANGLE_UNIT()
SI_UNIT($,.RADIAN.)
);
#8432=(
NAMED_UNIT(*)
SI_UNIT($,.STERADIAN.)
SOLID_ANGLE_UNIT()
);
#8451=SHAPE_DEFINITION_REPRESENTATION(#8476,#8532);
#8476=PRODUCT_DEFINITION_SHAPE('',$,#8558);
#8532=SHAPE_REPRESENTATION('',(#4280),#8421);
#8539=PRODUCT_DEFINITION_CONTEXT('part definition',#8616,'design');
#8558=PRODUCT_DEFINITION('Foot pad (1)','Foot pad (1)',#8583,
#8539);
#8583=PRODUCT_DEFINITION_FORMATION('',$,#8636);
#8616=APPLICATION_CONTEXT(
'Core Data for Automotive Mechanical Design Process');
#8617=PRODUCT_CONTEXT('part definition',#8616,'mechanical');
#8636=PRODUCT('Foot pad (1)','Foot pad (1)','Foot pad (1)',(#8617));
#8692=COLOUR_RGB('Sky Blue',0.24,0.69,0.87);
#8693=FILL_AREA_STYLE_COLOUR('',#8692);
#8694=FILL_AREA_STYLE('',(#8693));
#8695=SURFACE_STYLE_FILL_AREA(#8694);
#8696=SURFACE_SIDE_STYLE('',(#8695));
#8697=SURFACE_STYLE_USAGE(.BOTH.,#8696);
#8698=PRESENTATION_STYLE_ASSIGNMENT((#8697));
ENDSEC;
END-ISO-10303-21;
